ISO-10303-21;
HEADER;
/* Generated by software containing ST-Developer
 * from STEP Tools, Inc. (www.steptools.com) 
 */

FILE_DESCRIPTION(
/* description */ (''),
/* implementation_level */ '2;1');

FILE_NAME(
/* name */ '07_Outer_Bearing_Cup_L44610.step',
/* time_stamp */ '2026-10-25T01:26:34-07:00',
/* author */ (''),
/* organization */ (''),
/* preprocessor_version */ 'ST-DEVELOPER v20.2',
/* originating_system */ 'Autodesk Translation Framework v15.15.0.0',
/* authorisation */ '');

FILE_SCHEMA (('AUTOMOTIVE_DESIGN { 1 0 10303 214 3 1 1 }'));
ENDSEC;

DATA;
#10=MECHANICAL_DESIGN_GEOMETRIC_PRESENTATION_REPRESENTATION('',(#326),#71628);
#300=SHAPE_REPRESENTATION_RELATIONSHIP('SRR','None',#71688,#313);
#313=ADVANCED_BREP_SHAPE_REPRESENTATION('',(#339),#71620);
#326=STYLED_ITEM('',(#71818),#339);
#339=MANIFOLD_SOLID_BREP('Body1',#34213);
#1265=FACE_BOUND('',#6911,.T.);
#1266=FACE_BOUND('',#6916,.T.);
#2645=PLANE('',#36719);
#2646=PLANE('',#36727);
#3064=CYLINDRICAL_SURFACE('',#36715,25.146);
#4677=FACE_OUTER_BOUND('',#6907,.T.);
#4678=FACE_OUTER_BOUND('',#6908,.T.);
#4679=FACE_OUTER_BOUND('',#6909,.T.);
#4680=FACE_OUTER_BOUND('',#6910,.T.);
#4681=FACE_OUTER_BOUND('',#6912,.T.);
#4682=FACE_OUTER_BOUND('',#6913,.T.);
#4683=FACE_OUTER_BOUND('',#6914,.T.);
#4684=FACE_OUTER_BOUND('',#6915,.T.);
#6907=EDGE_LOOP('',(#29186,#29187,#29188,#29189));
#6908=EDGE_LOOP('',(#29190,#29191,#29192,#29193));
#6909=EDGE_LOOP('',(#29194,#29195,#29196,#29197));
#6910=EDGE_LOOP('',(#29198));
#6911=EDGE_LOOP('',(#29199));
#6912=EDGE_LOOP('',(#29200,#29201,#29202,#29203));
#6913=EDGE_LOOP('',(#29204,#29205,#29206,#29207));
#6914=EDGE_LOOP('',(#29208,#29209,#29210,#29211));
#6915=EDGE_LOOP('',(#29212));
#6916=EDGE_LOOP('',(#29213));
#9946=LINE('',#60087,#12996);
#9947=LINE('',#60092,#12997);
#9948=LINE('',#60096,#12998);
#9949=LINE('',#60102,#12999);
#9950=LINE('',#60106,#13000);
#9951=LINE('',#60110,#13001);
#12996=VECTOR('',#44771,24.746);
#12997=VECTOR('',#44778,25.146);
#12998=VECTOR('',#44783,24.846);
#12999=VECTOR('',#44790,23.9381298772848);
#13000=VECTOR('',#44795,23.0066610487235);
#13001=VECTOR('',#44800,22.4355961100811);
#14160=CIRCLE('',#36713,25.146);
#14161=CIRCLE('',#36714,24.346);
#14162=CIRCLE('',#36716,25.146);
#14163=CIRCLE('',#36718,24.546);
#14164=CIRCLE('',#36720,24.0881298772848);
#14165=CIRCLE('',#36722,23.7881298772848);
#14166=CIRCLE('',#36724,22.2251922201623);
#14167=CIRCLE('',#36726,22.646);
#16565=VERTEX_POINT('',#60084);
#16566=VERTEX_POINT('',#60086);
#16567=VERTEX_POINT('',#60090);
#16568=VERTEX_POINT('',#60094);
#16569=VERTEX_POINT('',#60098);
#16570=VERTEX_POINT('',#60101);
#16571=VERTEX_POINT('',#60105);
#16572=VERTEX_POINT('',#60109);
#20907=EDGE_CURVE('',#16565,#16565,#14160,.T.);
#20908=EDGE_CURVE('',#16565,#16566,#9946,.T.);
#20909=EDGE_CURVE('',#16566,#16566,#14161,.T.);
#20910=EDGE_CURVE('',#16567,#16567,#14162,.T.);
#20911=EDGE_CURVE('',#16567,#16565,#9947,.T.);
#20912=EDGE_CURVE('',#16568,#16568,#14163,.T.);
#20913=EDGE_CURVE('',#16568,#16567,#9948,.T.);
#20914=EDGE_CURVE('',#16569,#16569,#14164,.T.);
#20915=EDGE_CURVE('',#16569,#16570,#9949,.T.);
#20916=EDGE_CURVE('',#16570,#16570,#14165,.T.);
#20917=EDGE_CURVE('',#16570,#16571,#9950,.T.);
#20918=EDGE_CURVE('',#16571,#16571,#14166,.T.);
#20919=EDGE_CURVE('',#16571,#16572,#9951,.T.);
#20920=EDGE_CURVE('',#16572,#16572,#14167,.T.);
#29186=ORIENTED_EDGE('',*,*,#20907,.F.);
#29187=ORIENTED_EDGE('',*,*,#20908,.T.);
#29188=ORIENTED_EDGE('',*,*,#20909,.T.);
#29189=ORIENTED_EDGE('',*,*,#20908,.F.);
#29190=ORIENTED_EDGE('',*,*,#20910,.F.);
#29191=ORIENTED_EDGE('',*,*,#20911,.T.);
#29192=ORIENTED_EDGE('',*,*,#20907,.T.);
#29193=ORIENTED_EDGE('',*,*,#20911,.F.);
#29194=ORIENTED_EDGE('',*,*,#20912,.F.);
#29195=ORIENTED_EDGE('',*,*,#20913,.T.);
#29196=ORIENTED_EDGE('',*,*,#20910,.T.);
#29197=ORIENTED_EDGE('',*,*,#20913,.F.);
#29198=ORIENTED_EDGE('',*,*,#20912,.T.);
#29199=ORIENTED_EDGE('',*,*,#20914,.F.);
#29200=ORIENTED_EDGE('',*,*,#20914,.T.);
#29201=ORIENTED_EDGE('',*,*,#20915,.T.);
#29202=ORIENTED_EDGE('',*,*,#20916,.F.);
#29203=ORIENTED_EDGE('',*,*,#20915,.F.);
#29204=ORIENTED_EDGE('',*,*,#20916,.T.);
#29205=ORIENTED_EDGE('',*,*,#20917,.T.);
#29206=ORIENTED_EDGE('',*,*,#20918,.F.);
#29207=ORIENTED_EDGE('',*,*,#20917,.F.);
#29208=ORIENTED_EDGE('',*,*,#20918,.T.);
#29209=ORIENTED_EDGE('',*,*,#20919,.T.);
#29210=ORIENTED_EDGE('',*,*,#20920,.F.);
#29211=ORIENTED_EDGE('',*,*,#20919,.F.);
#29212=ORIENTED_EDGE('',*,*,#20909,.F.);
#29213=ORIENTED_EDGE('',*,*,#20920,.T.);
#32027=CONICAL_SURFACE('',#36712,24.746,0.785398163397449);
#32028=CONICAL_SURFACE('',#36717,24.846,0.785398163397448);
#32029=CONICAL_SURFACE('',#36721,23.9381298772848,0.785398163397445);
#32030=CONICAL_SURFACE('',#36723,23.0066610487235,0.15707963267949);
#32031=CONICAL_SURFACE('',#36725,22.4355961100811,0.699606280388887);
#33651=ADVANCED_FACE('',(#4677),#32027,.T.);
#33652=ADVANCED_FACE('',(#4678),#3064,.T.);
#33653=ADVANCED_FACE('',(#4679),#32028,.T.);
#33654=ADVANCED_FACE('',(#4680,#1265),#2645,.T.);
#33655=ADVANCED_FACE('',(#4681),#32029,.F.);
#33656=ADVANCED_FACE('',(#4682),#32030,.F.);
#33657=ADVANCED_FACE('',(#4683),#32031,.F.);
#33658=ADVANCED_FACE('',(#4684,#1266),#2646,.T.);
#34213=CLOSED_SHELL('',(#33651,#33652,#33653,#33654,#33655,#33656,#33657,
#33658));
#36711=AXIS2_PLACEMENT_3D('',#60082,#44765,#44766);
#36712=AXIS2_PLACEMENT_3D('',#60083,#44767,#44768);
#36713=AXIS2_PLACEMENT_3D('',#60085,#44769,#44770);
#36714=AXIS2_PLACEMENT_3D('',#60088,#44772,#44773);
#36715=AXIS2_PLACEMENT_3D('',#60089,#44774,#44775);
#36716=AXIS2_PLACEMENT_3D('',#60091,#44776,#44777);
#36717=AXIS2_PLACEMENT_3D('',#60093,#44779,#44780);
#36718=AXIS2_PLACEMENT_3D('',#60095,#44781,#44782);
#36719=AXIS2_PLACEMENT_3D('',#60097,#44784,#44785);
#36720=AXIS2_PLACEMENT_3D('',#60099,#44786,#44787);
#36721=AXIS2_PLACEMENT_3D('',#60100,#44788,#44789);
#36722=AXIS2_PLACEMENT_3D('',#60103,#44791,#44792);
#36723=AXIS2_PLACEMENT_3D('',#60104,#44793,#44794);
#36724=AXIS2_PLACEMENT_3D('',#60107,#44796,#44797);
#36725=AXIS2_PLACEMENT_3D('',#60108,#44798,#44799);
#36726=AXIS2_PLACEMENT_3D('',#60111,#44801,#44802);
#36727=AXIS2_PLACEMENT_3D('',#60112,#44803,#44804);
#44765=DIRECTION('axis',(0.,0.,1.));
#44766=DIRECTION('refdir',(1.,0.,0.));
#44767=DIRECTION('center_axis',(1.,0.,0.));
#44768=DIRECTION('ref_axis',(0.,1.,0.));
#44769=DIRECTION('center_axis',(1.,0.,0.));
#44770=DIRECTION('ref_axis',(0.,0.,-1.));
#44771=DIRECTION('',(-0.707106781186547,0.707106781186548,8.65956056235494E-17));
#44772=DIRECTION('center_axis',(1.,0.,0.));
#44773=DIRECTION('ref_axis',(0.,0.,-1.));
#44774=DIRECTION('center_axis',(1.,0.,0.));
#44775=DIRECTION('ref_axis',(0.,1.,0.));
#44776=DIRECTION('center_axis',(1.,0.,0.));
#44777=DIRECTION('ref_axis',(0.,0.,-1.));
#44778=DIRECTION('',(-1.,0.,0.));
#44779=DIRECTION('center_axis',(-1.,0.,0.));
#44780=DIRECTION('ref_axis',(0.,1.,0.));
#44781=DIRECTION('center_axis',(1.,0.,0.));
#44782=DIRECTION('ref_axis',(0.,0.,-1.));
#44783=DIRECTION('',(-0.707106781186548,-0.707106781186548,-8.65956056235493E-17));
#44784=DIRECTION('center_axis',(1.,0.,0.));
#44785=DIRECTION('ref_axis',(0.,0.,-1.));
#44786=DIRECTION('center_axis',(1.,0.,0.));
#44787=DIRECTION('ref_axis',(0.,0.,-1.));
#44788=DIRECTION('center_axis',(1.,0.,0.));
#44789=DIRECTION('ref_axis',(0.,1.,0.));
#44790=DIRECTION('',(-0.70710678118655,0.707106781186545,8.6595605623549E-17));
#44791=DIRECTION('center_axis',(1.,0.,0.));
#44792=DIRECTION('ref_axis',(0.,0.,-1.));
#44793=DIRECTION('center_axis',(1.,0.,0.));
#44794=DIRECTION('ref_axis',(0.,1.,0.));
#44795=DIRECTION('',(-0.987688340595138,0.156434465040231,1.91576966887847E-17));
#44796=DIRECTION('center_axis',(1.,0.,0.));
#44797=DIRECTION('ref_axis',(0.,0.,-1.));
#44798=DIRECTION('center_axis',(-1.,0.,0.));
#44799=DIRECTION('ref_axis',(0.,1.,0.));
#44800=DIRECTION('',(-0.765095769134171,-0.643916503945187,-7.88570285474627E-17));
#44801=DIRECTION('center_axis',(1.,0.,0.));
#44802=DIRECTION('ref_axis',(0.,0.,-1.));
#44803=DIRECTION('center_axis',(-1.,0.,0.));
#44804=DIRECTION('ref_axis',(0.,0.,1.));
#60082=CARTESIAN_POINT('',(0.,0.,0.));
#60083=CARTESIAN_POINT('Origin',(0.4,0.,0.));
#60084=CARTESIAN_POINT('',(0.8,-25.146,-3.07949684113593E-15));
#60085=CARTESIAN_POINT('Origin',(0.8,0.,0.));
#60086=CARTESIAN_POINT('',(-4.85722573273506E-16,-24.346,-2.98152509720415E-15));
#60087=CARTESIAN_POINT('',(0.4,-24.746,-3.03051096917004E-15));
#60088=CARTESIAN_POINT('Origin',(0.,0.,0.));
#60089=CARTESIAN_POINT('Origin',(5.434,0.,0.));
#60090=CARTESIAN_POINT('',(10.068,-25.146,-3.07949684113593E-15));
#60091=CARTESIAN_POINT('Origin',(10.068,0.,0.));
#60092=CARTESIAN_POINT('',(5.434,-25.146,-3.07949684113593E-15));
#60093=CARTESIAN_POINT('Origin',(10.368,0.,0.));
#60094=CARTESIAN_POINT('',(10.668,-24.546,-3.00601803318709E-15));
#60095=CARTESIAN_POINT('Origin',(10.668,0.,0.));
#60096=CARTESIAN_POINT('',(10.368,-24.846,-3.04275743716151E-15));
#60097=CARTESIAN_POINT('Origin',(10.668,24.0881298772848,0.));
#60098=CARTESIAN_POINT('',(10.668,-24.0881298772848,-2.94994511516625E-15));
#60099=CARTESIAN_POINT('Origin',(10.668,0.,0.));
#60100=CARTESIAN_POINT('Origin',(10.518,0.,0.));
#60101=CARTESIAN_POINT('',(10.368,-23.7881298772848,-2.91320571119183E-15));
#60102=CARTESIAN_POINT('',(10.518,-23.9381298772848,-2.93157541317904E-15));
#60103=CARTESIAN_POINT('Origin',(10.368,0.,0.));
#60104=CARTESIAN_POINT('Origin',(5.434,0.,0.));
#60105=CARTESIAN_POINT('',(0.5,-22.2251922201623,-2.72180105128564E-15));
#60106=CARTESIAN_POINT('',(5.434,-23.0066610487235,-2.81750338123874E-15));
#60107=CARTESIAN_POINT('Origin',(0.5,0.,0.));
#60108=CARTESIAN_POINT('Origin',(0.25,0.,0.));
#60109=CARTESIAN_POINT('',(6.24500451351651E-16,-22.646,-2.7733351413491E-15));
#60110=CARTESIAN_POINT('',(0.25,-22.4355961100811,-2.74756809631737E-15));
#60111=CARTESIAN_POINT('Origin',(0.,0.,0.));
#60112=CARTESIAN_POINT('Origin',(0.,24.346,0.));
#71605=UNCERTAINTY_MEASURE_WITH_UNIT(LENGTH_MEASURE(0.01),#71629,
'DISTANCE_ACCURACY_VALUE',
'Maximum model space distance between geometric entities at asserted c
onnectivities');
#71613=UNCERTAINTY_MEASURE_WITH_UNIT(LENGTH_MEASURE(0.01),#71629,
'DISTANCE_ACCURACY_VALUE',
'Maximum model space distance between geometric entities at asserted c
onnectivities');
#71620=(
GEOMETRIC_REPRESENTATION_CONTEXT(3)
GLOBAL_UNCERTAINTY_ASSIGNED_CONTEXT((#71605))
GLOBAL_UNIT_ASSIGNED_CONTEXT((#71629,#71631,#71632))
REPRESENTATION_CONTEXT('','3D')
);
#71628=(
GEOMETRIC_REPRESENTATION_CONTEXT(3)
GLOBAL_UNCERTAINTY_ASSIGNED_CONTEXT((#71613))
GLOBAL_UNIT_ASSIGNED_CONTEXT((#71629,#71631,#71632))
REPRESENTATION_CONTEXT('','3D')
);
#71629=(
LENGTH_UNIT()
NAMED_UNIT(*)
SI_UNIT(.MILLI.,.METRE.)
);
#71631=(
NAMED_UNIT(*)
PLANE_ANGLE_UNIT()
SI_UNIT($,.RADIAN.)
);
#71632=(
NAMED_UNIT(*)
SI_UNIT($,.STERADIAN.)
SOLID_ANGLE_UNIT()
);
#71639=SHAPE_DEFINITION_REPRESENTATION(#71653,#71688);
#71653=PRODUCT_DEFINITION_SHAPE('',$,#71703);
#71688=SHAPE_REPRESENTATION('',(#36711),#71620);
#71696=PRODUCT_DEFINITION_CONTEXT('part definition',#71740,'design');
#71703=PRODUCT_DEFINITION('2026-10-25-00-23-52-009',
'07_Outer_Bearing_Cup_L44610',#71717,#71696);
#71717=PRODUCT_DEFINITION_FORMATION('',$,#71748);
#71740=APPLICATION_CONTEXT(
'Core Data for Automotive Mechanical Design Process');
#71741=PRODUCT_CONTEXT('part definition',#71740,'mechanical');
#71748=PRODUCT('2026-10-25-00-23-52-009','07_Outer_Bearing_Cup_L44610',
$,(#71741));
#71812=COLOUR_RGB('Grey',0.48,0.52,0.57);
#71813=FILL_AREA_STYLE_COLOUR('',#71812);
#71814=FILL_AREA_STYLE('',(#71813));
#71815=SURFACE_STYLE_FILL_AREA(#71814);
#71816=SURFACE_SIDE_STYLE('',(#71815));
#71817=SURFACE_STYLE_USAGE(.BOTH.,#71816);
#71818=PRESENTATION_STYLE_ASSIGNMENT((#71817));
ENDSEC;
END-ISO-10303-21;
